ISO-10303-21;
HEADER;
FILE_DESCRIPTION (('STEP AP214'),
    '1' );
FILE_NAME ('plain washer (type a)_is_IS 2016 A- 14.step',
    '2026-10-26T19:46:16',
    ( '' ),
    ( '' ),
    'SwSTEP 2.0',
    'SolidWorks 2025',
    '' );
FILE_SCHEMA (( 'AUTOMOTIVE_DESIGN' ));
ENDSEC;

DATA;
#498=AXIS2_PLACEMENT_3D ( 'NONE', #69594, #73760, #22068 ) ;
#1632=ORIENTED_EDGE ( 'NONE', *, *, #26944, .F. ) ;
#1645=PLANE ( 'NONE',  #16886 ) ;
#2427=CIRCLE ( 'NONE', #22954, 7.000000000000000000 ) ;
#3298=LINE ( 'NONE', #71565, #14669 ) ;
#3572=FACE_OUTER_BOUND ( 'NONE', #74054, .T. ) ;
#3730=ORIENTED_EDGE ( 'NONE', *, *, #64012, .T. ) ;
#3731=ORIENTED_EDGE ( 'NONE', *, *, #20294, .F. ) ;
#4132=FACE_OUTER_BOUND ( 'NONE', #32860, .T. ) ;
#4137=EDGE_CURVE ( 'NONE', #59151, #22196, #2427, .T. ) ;
#4300=DIRECTION ( 'NONE',  ( -0.000000000000000000, 1.000000000000000000, -0.000000000000000000 ) ) ;
#4457=VECTOR ( 'NONE', #50770, 1000.000000000000000 ) ;
#4839=CIRCLE ( 'NONE', #26512, 7.000000000000000000 ) ;
#5572=ADVANCED_FACE ( 'NONE', ( #23690 ), #45957, .T. ) ;
#5656=PRODUCT_DEFINITION_FORMATION_WITH_SPECIFIED_SOURCE ( 'ANY', '', #54717, .NOT_KNOWN. ) ;
#5977=CARTESIAN_POINT ( 'NONE',  ( 0.000000000000000000, 0.000000000000000000, 0.000000000000000000 ) ) ;
#6405=DIRECTION ( 'NONE',  ( 0.000000000000000000, 0.000000000000000000, 1.000000000000000000 ) ) ;
#6792=ORIENTED_EDGE ( 'NONE', *, *, #56411, .F. ) ;
#7218=PRODUCT_DEFINITION ( 'UNKNOWN', '', #5656, #11599 ) ;
#7530=DIRECTION ( 'NONE',  ( 0.000000000000000000, 0.000000000000000000, 1.000000000000000000 ) ) ;
#8427=AXIS2_PLACEMENT_3D ( 'NONE', #32987, #4300, #72582 ) ;
#8474=DIRECTION ( 'NONE',  ( -0.000000000000000000, 1.000000000000000000, -0.000000000000000000 ) ) ;
#8857=CYLINDRICAL_SURFACE ( 'NONE', #26703, 7.000000000000000000 ) ;
#9378=ORIENTED_EDGE ( 'NONE', *, *, #15678, .F. ) ;
#10047=CARTESIAN_POINT ( 'NONE',  ( 8.572527594031473190E-16, 0.000000000000000000, -7.000000000000000000 ) ) ;
#10404=ORIENTED_EDGE ( 'NONE', *, *, #64986, .T. ) ;
#10541=FACE_BOUND ( 'NONE', #60079, .T. ) ;
#10874=SHAPE_DEFINITION_REPRESENTATION ( #43243, #64301 ) ;
#11166=CARTESIAN_POINT ( 'NONE',  ( 0.000000000000000000, 0.000000000000000000, 7.000000000000000000 ) ) ;
#11422=DIRECTION ( 'NONE',  ( 0.000000000000000000, 0.000000000000000000, 1.000000000000000000 ) ) ;
#11599=PRODUCT_DEFINITION_CONTEXT ( 'detailed design', #72242, 'design' ) ;
#12588=VECTOR ( 'NONE', #62521, 1000.000000000000000 ) ;
#13300=DIRECTION ( 'NONE',  ( 0.000000000000000000, 0.000000000000000000, 1.000000000000000000 ) ) ;
#14143=ADVANCED_FACE ( 'NONE', ( #3572 ), #8857, .F. ) ;
#14192=LINE ( 'NONE', #11166, #4457 ) ;
#14286=AXIS2_PLACEMENT_3D ( 'NONE', #29771, #46379, #6405 ) ;
#14669=VECTOR ( 'NONE', #25173, 1000.000000000000000 ) ;
#15049=CYLINDRICAL_SURFACE ( 'NONE', #43151, 7.000000000000000000 ) ;
#15547=CIRCLE ( 'NONE', #49256, 12.00000000000000000 ) ;
#15678=EDGE_CURVE ( 'NONE', #65025, #21899, #27414, .T. ) ;
#15811=PLANE ( 'NONE',  #19100 ) ;
#16122=AXIS2_PLACEMENT_3D ( 'NONE', #71077, #17934, #18676 ) ;
#16703=AXIS2_PLACEMENT_3D ( 'NONE', #62132, #33124, #56488 ) ;
#16886=AXIS2_PLACEMENT_3D ( 'NONE', #18976, #41980, #13300 ) ;
#16933=DIRECTION ( 'NONE',  ( 0.000000000000000000, -1.000000000000000000, 0.000000000000000000 ) ) ;
#17517=ORIENTED_EDGE ( 'NONE', *, *, #63465, .T. ) ;
#17934=DIRECTION ( 'NONE',  ( -0.000000000000000000, 1.000000000000000000, -0.000000000000000000 ) ) ;
#18472=DIRECTION ( 'NONE',  ( 0.000000000000000000, 0.000000000000000000, 1.000000000000000000 ) ) ;
#18676=DIRECTION ( 'NONE',  ( 0.000000000000000000, 0.000000000000000000, 1.000000000000000000 ) ) ;
#18692=ORIENTED_EDGE ( 'NONE', *, *, #20294, .T. ) ;
#18976=CARTESIAN_POINT ( 'NONE',  ( 7.000000000000000000, 0.000000000000000000, 0.000000000000000000 ) ) ;
#19065=VERTEX_POINT ( 'NONE', #34944 ) ;
#19100=AXIS2_PLACEMENT_3D ( 'NONE', #56202, #16933, #38847 ) ;
#19950=CARTESIAN_POINT ( 'NONE',  ( 0.000000000000000000, 0.000000000000000000, 7.000000000000000000 ) ) ;
#20294=EDGE_CURVE ( 'NONE', #19065, #22196, #3298, .T. ) ;
#21011=CARTESIAN_POINT ( 'NONE',  ( 1.469576158976823947E-15, 0.000000000000000000, -12.00000000000000000 ) ) ;
#21760=FACE_OUTER_BOUND ( 'NONE', #73641, .T. ) ;
#21775=CARTESIAN_POINT ( 'NONE',  ( 0.000000000000000000, -2.500000000000000000, 7.000000000000000000 ) ) ;
#21899=VERTEX_POINT ( 'NONE', #46410 ) ;
#22068=DIRECTION ( 'NONE',  ( 0.000000000000000000, 0.000000000000000000, 1.000000000000000000 ) ) ;
#22151=LINE ( 'NONE', #45178, #12588 ) ;
#22196=VERTEX_POINT ( 'NONE', #10047 ) ;
#22259=EDGE_CURVE ( 'NONE', #73307, #59151, #14192, .T. ) ;
#22954=AXIS2_PLACEMENT_3D ( 'NONE', #56161, #33533, #32022 ) ;
#23523=CARTESIAN_POINT ( 'NONE',  ( 0.000000000000000000, 0.000000000000000000, 12.00000000000000000 ) ) ;
#23690=FACE_OUTER_BOUND ( 'NONE', #37039, .T. ) ;
#25173=DIRECTION ( 'NONE',  ( -0.000000000000000000, 1.000000000000000000, -0.000000000000000000 ) ) ;
#26015=ORIENTED_EDGE ( 'NONE', *, *, #64986, .F. ) ;
#26336=EDGE_CURVE ( 'NONE', #30502, #21899, #73396, .T. ) ;
#26512=AXIS2_PLACEMENT_3D ( 'NONE', #36202, #59219, #7530 ) ;
#26703=AXIS2_PLACEMENT_3D ( 'NONE', #60154, #8474, #37151 ) ;
#26944=EDGE_CURVE ( 'NONE', #41193, #65025, #15547, .T. ) ;
#27414=LINE ( 'NONE', #21011, #68757 ) ;
#27636=CARTESIAN_POINT ( 'NONE',  ( 0.000000000000000000, -2.500000000000000000, 0.000000000000000000 ) ) ;
#28899=CIRCLE ( 'NONE', #8427, 12.00000000000000000 ) ;
#28980=DIRECTION ( 'NONE',  ( -0.000000000000000000, 1.000000000000000000, -0.000000000000000000 ) ) ;
#29771=CARTESIAN_POINT ( 'NONE',  ( 0.000000000000000000, 0.000000000000000000, 0.000000000000000000 ) ) ;
#29933=FACE_OUTER_BOUND ( 'NONE', #58972, .T. ) ;
#30076=( NAMED_UNIT ( * ) SI_UNIT ( $, .STERADIAN. ) SOLID_ANGLE_UNIT ( ) );
#30502=VERTEX_POINT ( 'NONE', #23523 ) ;
#30690=ADVANCED_FACE ( 'NONE', ( #29933, #52949 ), #1645, .T. ) ;
#31403=AXIS2_PLACEMENT_3D ( 'NONE', #5977, #28980, #45584 ) ;
#32022=DIRECTION ( 'NONE',  ( 0.000000000000000000, 0.000000000000000000, 1.000000000000000000 ) ) ;
#32244=ORIENTED_EDGE ( 'NONE', *, *, #15678, .T. ) ;
#32779=( LENGTH_UNIT ( ) NAMED_UNIT ( * ) SI_UNIT ( .MILLI., .METRE. ) );
#32860=EDGE_LOOP ( 'NONE', ( #3731, #52577, #73770, #59425 ) ) ;
#32987=CARTESIAN_POINT ( 'NONE',  ( 0.000000000000000000, 0.000000000000000000, 0.000000000000000000 ) ) ;
#33124=DIRECTION ( 'NONE',  ( -0.000000000000000000, 1.000000000000000000, -0.000000000000000000 ) ) ;
#33533=DIRECTION ( 'NONE',  ( -0.000000000000000000, 1.000000000000000000, -0.000000000000000000 ) ) ;
#34130=ORIENTED_EDGE ( 'NONE', *, *, #4137, .F. ) ;
#34459=DIRECTION ( 'NONE',  ( 1.000000000000000000, 0.000000000000000000, 0.000000000000000000 ) ) ;
#34877=ORIENTED_EDGE ( 'NONE', *, *, #39412, .T. ) ;
#34944=CARTESIAN_POINT ( 'NONE',  ( 8.572527594031473190E-16, -2.500000000000000000, -7.000000000000000000 ) ) ;
#36202=CARTESIAN_POINT ( 'NONE',  ( 0.000000000000000000, -2.500000000000000000, 0.000000000000000000 ) ) ;
#36906=EDGE_LOOP ( 'NONE', ( #34130, #66183 ) ) ;
#37039=EDGE_LOOP ( 'NONE', ( #9378, #17517, #10404, #71998 ) ) ;
#37151=DIRECTION ( 'NONE',  ( 0.000000000000000000, 0.000000000000000000, 1.000000000000000000 ) ) ;
#38847=DIRECTION ( 'NONE',  ( 0.000000000000000000, -0.000000000000000000, -1.000000000000000000 ) ) ;
#39412=EDGE_CURVE ( 'NONE', #22196, #59151, #55110, .T. ) ;
#39691=ORIENTED_EDGE ( 'NONE', *, *, #26336, .F. ) ;
#41193=VERTEX_POINT ( 'NONE', #46062 ) ;
#41407=APPLICATION_CONTEXT ( 'automotive_design' ) ;
#41830=CLOSED_SHELL ( 'NONE', ( #61547, #14143, #60200, #30690, #5572, #61126 ) ) ;
#41980=DIRECTION ( 'NONE',  ( -0.000000000000000000, 1.000000000000000000, 0.000000000000000000 ) ) ;
#43151=AXIS2_PLACEMENT_3D ( 'NONE', #73518, #61460, #45594 ) ;
#43243=PRODUCT_DEFINITION_SHAPE ( 'NONE', 'NONE',  #7218 ) ;
#43554=ORIENTED_EDGE ( 'NONE', *, *, #56599, .T. ) ;
#43820=CIRCLE ( 'NONE', #498, 7.000000000000000000 ) ;
#44151=( GEOMETRIC_REPRESENTATION_CONTEXT ( 3 ) GLOBAL_UNCERTAINTY_ASSIGNED_CONTEXT ( ( #58487 ) ) GLOBAL_UNIT_ASSIGNED_CONTEXT ( ( #51319, #57744, #57368 ) ) REPRESENTATION_CONTEXT ( 'NONE', 'WORKASPACE' ) );
#44789=CYLINDRICAL_SURFACE ( 'NONE', #16703, 12.00000000000000000 ) ;
#44924=SHAPE_REPRESENTATION_RELATIONSHIP ( 'NONE' , 'NONE' ,  #64301, #53434 ) ;
#45178=CARTESIAN_POINT ( 'NONE',  ( 0.000000000000000000, 0.000000000000000000, 12.00000000000000000 ) ) ;
#45584=DIRECTION ( 'NONE',  ( 0.000000000000000000, 0.000000000000000000, 1.000000000000000000 ) ) ;
#45594=DIRECTION ( 'NONE',  ( 0.000000000000000000, 0.000000000000000000, 1.000000000000000000 ) ) ;
#45957=CYLINDRICAL_SURFACE ( 'NONE', #31403, 12.00000000000000000 ) ;
#46062=CARTESIAN_POINT ( 'NONE',  ( 0.000000000000000000, -2.500000000000000000, 12.00000000000000000 ) ) ;
#46379=DIRECTION ( 'NONE',  ( -0.000000000000000000, 1.000000000000000000, -0.000000000000000000 ) ) ;
#46410=CARTESIAN_POINT ( 'NONE',  ( 1.469576158976823947E-15, 0.000000000000000000, -12.00000000000000000 ) ) ;
#49256=AXIS2_PLACEMENT_3D ( 'NONE', #27636, #51023, #68002 ) ;
#50770=DIRECTION ( 'NONE',  ( -0.000000000000000000, 1.000000000000000000, -0.000000000000000000 ) ) ;
#51023=DIRECTION ( 'NONE',  ( -0.000000000000000000, 1.000000000000000000, -0.000000000000000000 ) ) ;
#51319=( LENGTH_UNIT ( ) NAMED_UNIT ( * ) SI_UNIT ( .MILLI., .METRE. ) );
#52577=ORIENTED_EDGE ( 'NONE', *, *, #64012, .F. ) ;
#52949=FACE_BOUND ( 'NONE', #36906, .T. ) ;
#53434=ADVANCED_BREP_SHAPE_REPRESENTATION ( '', ( #66045, #57354 ), #44151 ) ;
#54083=UNCERTAINTY_MEASURE_WITH_UNIT (LENGTH_MEASURE( 1.000000000000000082E-05 ), #32779, 'distance_accuracy_value', 'NONE');
#54717=PRODUCT ( 'plain washer (type a)_is_IS 2016 A- 14', 'plain washer (type a)_is_IS 2016 A- 14', '', ( #57659 ) ) ;
#55110=CIRCLE ( 'NONE', #57480, 7.000000000000000000 ) ;
#56161=CARTESIAN_POINT ( 'NONE',  ( 0.000000000000000000, 0.000000000000000000, 0.000000000000000000 ) ) ;
#56202=CARTESIAN_POINT ( 'NONE',  ( 7.000000000000000000, -2.500000000000000000, 0.000000000000000000 ) ) ;
#56318=ORIENTED_EDGE ( 'NONE', *, *, #56411, .T. ) ;
#56411=EDGE_CURVE ( 'NONE', #19065, #73307, #4839, .T. ) ;
#56488=DIRECTION ( 'NONE',  ( 0.000000000000000000, 0.000000000000000000, 1.000000000000000000 ) ) ;
#56599=EDGE_CURVE ( 'NONE', #21899, #30502, #28899, .T. ) ;
#57354=AXIS2_PLACEMENT_3D ( 'NONE', #63097, #11422, #34459 ) ;
#57368=( NAMED_UNIT ( * ) SI_UNIT ( $, .STERADIAN. ) SOLID_ANGLE_UNIT ( ) );
#57480=AXIS2_PLACEMENT_3D ( 'NONE', #70165, #70523, #18472 ) ;
#57659=PRODUCT_CONTEXT ( 'NONE', #41407, 'mechanical' ) ;
#57744=( NAMED_UNIT ( * ) PLANE_ANGLE_UNIT ( ) SI_UNIT ( $, .RADIAN. ) );
#57946=ORIENTED_EDGE ( 'NONE', *, *, #22259, .F. ) ;
#58487=UNCERTAINTY_MEASURE_WITH_UNIT (LENGTH_MEASURE( 1.000000000000000082E-05 ), #51319, 'distance_accuracy_value', 'NONE');
#58972=EDGE_LOOP ( 'NONE', ( #63906, #43554 ) ) ;
#59151=VERTEX_POINT ( 'NONE', #19950 ) ;
#59219=DIRECTION ( 'NONE',  ( -0.000000000000000000, 1.000000000000000000, -0.000000000000000000 ) ) ;
#59425=ORIENTED_EDGE ( 'NONE', *, *, #4137, .T. ) ;
#59502=CIRCLE ( 'NONE', #16122, 12.00000000000000000 ) ;
#60079=EDGE_LOOP ( 'NONE', ( #3730, #56318 ) ) ;
#60154=CARTESIAN_POINT ( 'NONE',  ( 0.000000000000000000, 0.000000000000000000, 0.000000000000000000 ) ) ;
#60200=ADVANCED_FACE ( 'NONE', ( #4132 ), #15049, .F. ) ;
#60840=MECHANICAL_DESIGN_GEOMETRIC_PRESENTATION_REPRESENTATION('',(#70434),#66817);
#61126=ADVANCED_FACE ( 'NONE', ( #10541, #62215 ), #15811, .T. ) ;
#61460=DIRECTION ( 'NONE',  ( -0.000000000000000000, 1.000000000000000000, -0.000000000000000000 ) ) ;
#61547=ADVANCED_FACE ( 'NONE', ( #21760 ), #44789, .T. ) ;
#62132=CARTESIAN_POINT ( 'NONE',  ( 0.000000000000000000, 0.000000000000000000, 0.000000000000000000 ) ) ;
#62215=FACE_OUTER_BOUND ( 'NONE', #65667, .T. ) ;
#62521=DIRECTION ( 'NONE',  ( -0.000000000000000000, 1.000000000000000000, -0.000000000000000000 ) ) ;
#63097=CARTESIAN_POINT ( 'NONE',  ( 0.000000000000000000, 0.000000000000000000, 0.000000000000000000 ) ) ;
#63465=EDGE_CURVE ( 'NONE', #65025, #41193, #59502, .T. ) ;
#63906=ORIENTED_EDGE ( 'NONE', *, *, #26336, .T. ) ;
#64012=EDGE_CURVE ( 'NONE', #73307, #19065, #43820, .T. ) ;
#64301=SHAPE_REPRESENTATION ( 'plain washer (type a)_is_IS 2016 A- 14', ( #57354 ), #44151 ) ;
#64986=EDGE_CURVE ( 'NONE', #41193, #30502, #22151, .T. ) ;
#65025=VERTEX_POINT ( 'NONE', #71137 ) ;
#65667=EDGE_LOOP ( 'NONE', ( #1632, #67648 ) ) ;
#66045=MANIFOLD_SOLID_BREP ( 'BaseBody', #41830 ) ;
#66183=ORIENTED_EDGE ( 'NONE', *, *, #39412, .F. ) ;
#66292=DIRECTION ( 'NONE',  ( -0.000000000000000000, 1.000000000000000000, -0.000000000000000000 ) ) ;
#66817=( GEOMETRIC_REPRESENTATION_CONTEXT ( 3 ) GLOBAL_UNCERTAINTY_ASSIGNED_CONTEXT ( ( #54083 ) ) GLOBAL_UNIT_ASSIGNED_CONTEXT ( ( #32779, #73126, #30076 ) ) REPRESENTATION_CONTEXT ( 'NONE', 'WORKASPACE' ) );
#67648=ORIENTED_EDGE ( 'NONE', *, *, #63465, .F. ) ;
#68002=DIRECTION ( 'NONE',  ( 0.000000000000000000, 0.000000000000000000, 1.000000000000000000 ) ) ;
#68757=VECTOR ( 'NONE', #66292, 1000.000000000000000 ) ;
#69594=CARTESIAN_POINT ( 'NONE',  ( 0.000000000000000000, -2.500000000000000000, 0.000000000000000000 ) ) ;
#70165=CARTESIAN_POINT ( 'NONE',  ( 0.000000000000000000, 0.000000000000000000, 0.000000000000000000 ) ) ;
#70434=STYLED_ITEM('',(#74706),#66045);
#70523=DIRECTION ( 'NONE',  ( -0.000000000000000000, 1.000000000000000000, -0.000000000000000000 ) ) ;
#71077=CARTESIAN_POINT ( 'NONE',  ( 0.000000000000000000, -2.500000000000000000, 0.000000000000000000 ) ) ;
#71137=CARTESIAN_POINT ( 'NONE',  ( 1.469576158976823947E-15, -2.500000000000000000, -12.00000000000000000 ) ) ;
#71565=CARTESIAN_POINT ( 'NONE',  ( 8.572527594031473190E-16, 0.000000000000000000, -7.000000000000000000 ) ) ;
#71998=ORIENTED_EDGE ( 'NONE', *, *, #56599, .F. ) ;
#72242=APPLICATION_CONTEXT ( 'automotive_design' ) ;
#72582=DIRECTION ( 'NONE',  ( 0.000000000000000000, 0.000000000000000000, 1.000000000000000000 ) ) ;
#73126=( NAMED_UNIT ( * ) PLANE_ANGLE_UNIT ( ) SI_UNIT ( $, .RADIAN. ) );
#73307=VERTEX_POINT ( 'NONE', #21775 ) ;
#73396=CIRCLE ( 'NONE', #14286, 12.00000000000000000 ) ;
#73518=CARTESIAN_POINT ( 'NONE',  ( 0.000000000000000000, 0.000000000000000000, 0.000000000000000000 ) ) ;
#73641=EDGE_LOOP ( 'NONE', ( #74513, #32244, #39691, #26015 ) ) ;
#73760=DIRECTION ( 'NONE',  ( -0.000000000000000000, 1.000000000000000000, -0.000000000000000000 ) ) ;
#73770=ORIENTED_EDGE ( 'NONE', *, *, #22259, .T. ) ;
#74054=EDGE_LOOP ( 'NONE', ( #6792, #18692, #34877, #57946 ) ) ;
#74513=ORIENTED_EDGE ( 'NONE', *, *, #26944, .T. ) ;
#74700=COLOUR_RGB('Black',0.12,0.14,0.17);
#74701=FILL_AREA_STYLE_COLOUR('',#74700);
#74702=FILL_AREA_STYLE('',(#74701));
#74703=SURFACE_STYLE_FILL_AREA(#74702);
#74704=SURFACE_SIDE_STYLE('',(#74703));
#74705=SURFACE_STYLE_USAGE(.BOTH.,#74704);
#74706=PRESENTATION_STYLE_ASSIGNMENT((#74705));
ENDSEC;
END-ISO-10303-21;
